ISO-10303-21;
HEADER;
/* Generated by software containing ST-Developer
 * from STEP Tools, Inc. (www.steptools.com) 
 */

FILE_DESCRIPTION(
/* description */ ('Belt tension measurement rig'),
/* implementation_level */ '2;1');

FILE_NAME(
/* name */ 'Input M3 set screw.step',
/* time_stamp */ '2026-10-28T03:24:44-07:00',
/* author */ (''),
/* organization */ (''),
/* preprocessor_version */ 'ST-DEVELOPER v20.2',
/* originating_system */ 'Autodesk Translation Framework v15.17.0.0',
/* authorisation */ '');

FILE_SCHEMA (('AUTOMOTIVE_DESIGN { 1 0 10303 214 3 1 1 }'));
ENDSEC;

DATA;
#10=MECHANICAL_DESIGN_GEOMETRIC_PRESENTATION_REPRESENTATION('',(#747),#23587);
#622=SHAPE_REPRESENTATION_RELATIONSHIP('SRR','None',#23872,#677);
#677=ADVANCED_BREP_SHAPE_REPRESENTATION('',(#815),#23570);
#747=STYLED_ITEM('',(#24218),#815);
#815=MANIFOLD_SOLID_BREP('Body1',#12254);
#1288=PLANE('',#13854);
#1289=PLANE('',#13855);
#1820=FACE_OUTER_BOUND('',#2688,.T.);
#1821=FACE_OUTER_BOUND('',#2689,.T.);
#1822=FACE_OUTER_BOUND('',#2690,.T.);
#2688=EDGE_LOOP('',(#9980,#9981,#9982,#9983));
#2689=EDGE_LOOP('',(#9984));
#2690=EDGE_LOOP('',(#9985));
#3503=LINE('',#21521,#4254);
#4254=VECTOR('',#17006,0.15);
#4916=CIRCLE('',#13852,0.15);
#4917=CIRCLE('',#13853,0.15);
#5931=VERTEX_POINT('',#21518);
#5932=VERTEX_POINT('',#21520);
#7349=EDGE_CURVE('',#5931,#5931,#4916,.T.);
#7350=EDGE_CURVE('',#5931,#5932,#3503,.T.);
#7351=EDGE_CURVE('',#5932,#5932,#4917,.T.);
#9980=ORIENTED_EDGE('',*,*,#7349,.F.);
#9981=ORIENTED_EDGE('',*,*,#7350,.T.);
#9982=ORIENTED_EDGE('',*,*,#7351,.T.);
#9983=ORIENTED_EDGE('',*,*,#7350,.F.);
#9984=ORIENTED_EDGE('',*,*,#7349,.T.);
#9985=ORIENTED_EDGE('',*,*,#7351,.F.);
#11327=CYLINDRICAL_SURFACE('',#13851,0.15);
#11961=ADVANCED_FACE('',(#1820),#11327,.T.);
#11962=ADVANCED_FACE('',(#1821),#1288,.T.);
#11963=ADVANCED_FACE('',(#1822),#1289,.F.);
#12254=CLOSED_SHELL('',(#11961,#11962,#11963));
#13850=AXIS2_PLACEMENT_3D('',#21516,#17000,#17001);
#13851=AXIS2_PLACEMENT_3D('',#21517,#17002,#17003);
#13852=AXIS2_PLACEMENT_3D('',#21519,#17004,#17005);
#13853=AXIS2_PLACEMENT_3D('',#21522,#17007,#17008);
#13854=AXIS2_PLACEMENT_3D('',#21523,#17009,#17010);
#13855=AXIS2_PLACEMENT_3D('',#21524,#17011,#17012);
#17000=DIRECTION('axis',(0.,0.,1.));
#17001=DIRECTION('refdir',(1.,0.,0.));
#17002=DIRECTION('center_axis',(0.,0.,1.));
#17003=DIRECTION('ref_axis',(1.,0.,0.));
#17004=DIRECTION('center_axis',(0.,0.,1.));
#17005=DIRECTION('ref_axis',(1.,0.,0.));
#17006=DIRECTION('',(0.,0.,-1.));
#17007=DIRECTION('center_axis',(0.,0.,1.));
#17008=DIRECTION('ref_axis',(1.,0.,0.));
#17009=DIRECTION('center_axis',(0.,0.,1.));
#17010=DIRECTION('ref_axis',(1.,0.,0.));
#17011=DIRECTION('center_axis',(0.,0.,1.));
#17012=DIRECTION('ref_axis',(1.,0.,0.));
#21516=CARTESIAN_POINT('',(0.,0.,0.));
#21517=CARTESIAN_POINT('Origin',(0.,-3.95,6.35));
#21518=CARTESIAN_POINT('',(-0.15,-3.95,6.6));
#21519=CARTESIAN_POINT('Origin',(0.,-3.95,6.6));
#21520=CARTESIAN_POINT('',(-0.15,-3.95,6.35));
#21521=CARTESIAN_POINT('',(-0.15,-3.95,6.35));
#21522=CARTESIAN_POINT('Origin',(0.,-3.95,6.35));
#21523=CARTESIAN_POINT('Origin',(0.,-3.95,6.6));
#21524=CARTESIAN_POINT('Origin',(0.,-3.95,6.35));
#23505=UNCERTAINTY_MEASURE_WITH_UNIT(LENGTH_MEASURE(0.001),#23588,
'DISTANCE_ACCURACY_VALUE',
'Maximum model space distance between geometric entities at asserted c
onnectivities');
#23522=UNCERTAINTY_MEASURE_WITH_UNIT(LENGTH_MEASURE(0.001),#23588,
'DISTANCE_ACCURACY_VALUE',
'Maximum model space distance between geometric entities at asserted c
onnectivities');
#23570=(
GEOMETRIC_REPRESENTATION_CONTEXT(3)
GLOBAL_UNCERTAINTY_ASSIGNED_CONTEXT((#23505))
GLOBAL_UNIT_ASSIGNED_CONTEXT((#23588,#23590,#23591))
REPRESENTATION_CONTEXT('','3D')
);
#23587=(
GEOMETRIC_REPRESENTATION_CONTEXT(3)
GLOBAL_UNCERTAINTY_ASSIGNED_CONTEXT((#23522))
GLOBAL_UNIT_ASSIGNED_CONTEXT((#23588,#23590,#23591))
REPRESENTATION_CONTEXT('','3D')
);
#23588=(
LENGTH_UNIT()
NAMED_UNIT(*)
SI_UNIT(.CENTI.,.METRE.)
);
#23590=(
NAMED_UNIT(*)
PLANE_ANGLE_UNIT()
SI_UNIT($,.RADIAN.)
);
#23591=(
NAMED_UNIT(*)
SI_UNIT($,.STERADIAN.)
SOLID_ANGLE_UNIT()
);
#23639=SHAPE_DEFINITION_REPRESENTATION(#23716,#23872);
#23716=PRODUCT_DEFINITION_SHAPE('',$,#23937);
#23872=SHAPE_REPRESENTATION('',(#13850),#23570);
#23889=PRODUCT_DEFINITION_CONTEXT('part definition',#24083,'design');
#23937=PRODUCT_DEFINITION('Input M3 set screw','Input M3 set screw',#24001,
#23889);
#24001=PRODUCT_DEFINITION_FORMATION('',$,#24132);
#24083=APPLICATION_CONTEXT(
'Core Data for Automotive Mechanical Design Process');
#24084=PRODUCT_CONTEXT('part definition',#24083,'mechanical');
#24132=PRODUCT('Input M3 set screw','Input M3 set screw',
'Input M3 set screw',(#24084));
#24212=COLOUR_RGB('Black',0.12,0.14,0.17);
#24213=FILL_AREA_STYLE_COLOUR('',#24212);
#24214=FILL_AREA_STYLE('',(#24213));
#24215=SURFACE_STYLE_FILL_AREA(#24214);
#24216=SURFACE_SIDE_STYLE('',(#24215));
#24217=SURFACE_STYLE_USAGE(.BOTH.,#24216);
#24218=PRESENTATION_STYLE_ASSIGNMENT((#24217));
ENDSEC;
END-ISO-10303-21;
